ISO-10303-21;
HEADER;
/* Generated by software containing ST-Developer
 * from STEP Tools, Inc. (www.steptools.com) 
 */

FILE_DESCRIPTION(
/* description */ ('Worm-less right-angle friction wheel drive'),
/* implementation_level */ '2;1');

FILE_NAME(
/* name */ 'Bearing cap (6).step',
/* time_stamp */ '2026-10-28T03:22:36-07:00',
/* author */ (''),
/* organization */ (''),
/* preprocessor_version */ 'ST-DEVELOPER v20.2',
/* originating_system */ 'Autodesk Translation Framework v15.17.0.0',
/* authorisation */ '');

FILE_SCHEMA (('AUTOMOTIVE_DESIGN { 1 0 10303 214 3 1 1 }'));
ENDSEC;

DATA;
#10=MECHANICAL_DESIGN_GEOMETRIC_PRESENTATION_REPRESENTATION('',(#625),#17046);
#531=SHAPE_REPRESENTATION_RELATIONSHIP('SRR','None',#17274,#578);
#578=ADVANCED_BREP_SHAPE_REPRESENTATION('',(#679),#17010);
#625=STYLED_ITEM('',(#17591),#679);
#679=MANIFOLD_SOLID_BREP('Body1',#8180);
#873=FACE_BOUND('',#2020,.T.);
#874=FACE_BOUND('',#2024,.T.);
#875=FACE_BOUND('',#2025,.T.);
#876=FACE_BOUND('',#2026,.T.);
#877=FACE_BOUND('',#2027,.T.);
#878=FACE_BOUND('',#2028,.T.);
#879=FACE_BOUND('',#2030,.T.);
#880=FACE_BOUND('',#2031,.T.);
#881=FACE_BOUND('',#2032,.T.);
#882=FACE_BOUND('',#2033,.T.);
#883=FACE_BOUND('',#2034,.T.);
#1042=PLANE('',#9140);
#1043=PLANE('',#9147);
#1044=PLANE('',#9148);
#1390=FACE_OUTER_BOUND('',#2014,.T.);
#1391=FACE_OUTER_BOUND('',#2015,.T.);
#1392=FACE_OUTER_BOUND('',#2016,.T.);
#1393=FACE_OUTER_BOUND('',#2017,.T.);
#1394=FACE_OUTER_BOUND('',#2018,.T.);
#1395=FACE_OUTER_BOUND('',#2019,.T.);
#1396=FACE_OUTER_BOUND('',#2021,.T.);
#1397=FACE_OUTER_BOUND('',#2022,.T.);
#1398=FACE_OUTER_BOUND('',#2023,.T.);
#1399=FACE_OUTER_BOUND('',#2029,.T.);
#2014=EDGE_LOOP('',(#6422,#6423,#6424,#6425));
#2015=EDGE_LOOP('',(#6426,#6427,#6428,#6429));
#2016=EDGE_LOOP('',(#6430,#6431,#6432,#6433));
#2017=EDGE_LOOP('',(#6434,#6435,#6436,#6437));
#2018=EDGE_LOOP('',(#6438,#6439,#6440,#6441));
#2019=EDGE_LOOP('',(#6442));
#2020=EDGE_LOOP('',(#6443));
#2021=EDGE_LOOP('',(#6444,#6445,#6446,#6447));
#2022=EDGE_LOOP('',(#6448,#6449,#6450,#6451));
#2023=EDGE_LOOP('',(#6452));
#2024=EDGE_LOOP('',(#6453));
#2025=EDGE_LOOP('',(#6454));
#2026=EDGE_LOOP('',(#6455));
#2027=EDGE_LOOP('',(#6456));
#2028=EDGE_LOOP('',(#6457));
#2029=EDGE_LOOP('',(#6458));
#2030=EDGE_LOOP('',(#6459));
#2031=EDGE_LOOP('',(#6460));
#2032=EDGE_LOOP('',(#6461));
#2033=EDGE_LOOP('',(#6462));
#2034=EDGE_LOOP('',(#6463));
#2637=LINE('',#13318,#3177);
#2638=LINE('',#13324,#3178);
#2639=LINE('',#13330,#3179);
#2640=LINE('',#13336,#3180);
#2641=LINE('',#13342,#3181);
#2642=LINE('',#13349,#3182);
#2643=LINE('',#13355,#3183);
#3177=VECTOR('',#10803,0.225);
#3178=VECTOR('',#10810,0.225);
#3179=VECTOR('',#10817,0.225);
#3180=VECTOR('',#10824,0.225);
#3181=VECTOR('',#10831,1.59);
#3182=VECTOR('',#10840,1.2);
#3183=VECTOR('',#10847,2.4);
#3641=CIRCLE('',#9126,0.225);
#3642=CIRCLE('',#9127,0.225);
#3643=CIRCLE('',#9129,0.225);
#3644=CIRCLE('',#9130,0.225);
#3645=CIRCLE('',#9132,0.225);
#3646=CIRCLE('',#9133,0.225);
#3647=CIRCLE('',#9135,0.225);
#3648=CIRCLE('',#9136,0.225);
#3649=CIRCLE('',#9138,1.59);
#3650=CIRCLE('',#9139,1.59);
#3651=CIRCLE('',#9141,1.2);
#3652=CIRCLE('',#9143,1.2);
#3653=CIRCLE('',#9145,2.4);
#3654=CIRCLE('',#9146,2.4);
#4165=VERTEX_POINT('',#13315);
#4166=VERTEX_POINT('',#13317);
#4167=VERTEX_POINT('',#13321);
#4168=VERTEX_POINT('',#13323);
#4169=VERTEX_POINT('',#13327);
#4170=VERTEX_POINT('',#13329);
#4171=VERTEX_POINT('',#13333);
#4172=VERTEX_POINT('',#13335);
#4173=VERTEX_POINT('',#13339);
#4174=VERTEX_POINT('',#13341);
#4175=VERTEX_POINT('',#13345);
#4176=VERTEX_POINT('',#13348);
#4177=VERTEX_POINT('',#13352);
#4178=VERTEX_POINT('',#13354);
#4980=EDGE_CURVE('',#4165,#4165,#3641,.T.);
#4981=EDGE_CURVE('',#4165,#4166,#2637,.T.);
#4982=EDGE_CURVE('',#4166,#4166,#3642,.T.);
#4983=EDGE_CURVE('',#4167,#4167,#3643,.T.);
#4984=EDGE_CURVE('',#4167,#4168,#2638,.T.);
#4985=EDGE_CURVE('',#4168,#4168,#3644,.T.);
#4986=EDGE_CURVE('',#4169,#4169,#3645,.T.);
#4987=EDGE_CURVE('',#4169,#4170,#2639,.T.);
#4988=EDGE_CURVE('',#4170,#4170,#3646,.T.);
#4989=EDGE_CURVE('',#4171,#4171,#3647,.T.);
#4990=EDGE_CURVE('',#4171,#4172,#2640,.T.);
#4991=EDGE_CURVE('',#4172,#4172,#3648,.T.);
#4992=EDGE_CURVE('',#4173,#4173,#3649,.T.);
#4993=EDGE_CURVE('',#4173,#4174,#2641,.T.);
#4994=EDGE_CURVE('',#4174,#4174,#3650,.T.);
#4995=EDGE_CURVE('',#4175,#4175,#3651,.T.);
#4996=EDGE_CURVE('',#4175,#4176,#2642,.T.);
#4997=EDGE_CURVE('',#4176,#4176,#3652,.T.);
#4998=EDGE_CURVE('',#4177,#4177,#3653,.T.);
#4999=EDGE_CURVE('',#4177,#4178,#2643,.T.);
#5000=EDGE_CURVE('',#4178,#4178,#3654,.T.);
#6422=ORIENTED_EDGE('',*,*,#4980,.F.);
#6423=ORIENTED_EDGE('',*,*,#4981,.T.);
#6424=ORIENTED_EDGE('',*,*,#4982,.F.);
#6425=ORIENTED_EDGE('',*,*,#4981,.F.);
#6426=ORIENTED_EDGE('',*,*,#4983,.F.);
#6427=ORIENTED_EDGE('',*,*,#4984,.T.);
#6428=ORIENTED_EDGE('',*,*,#4985,.F.);
#6429=ORIENTED_EDGE('',*,*,#4984,.F.);
#6430=ORIENTED_EDGE('',*,*,#4986,.F.);
#6431=ORIENTED_EDGE('',*,*,#4987,.T.);
#6432=ORIENTED_EDGE('',*,*,#4988,.F.);
#6433=ORIENTED_EDGE('',*,*,#4987,.F.);
#6434=ORIENTED_EDGE('',*,*,#4989,.F.);
#6435=ORIENTED_EDGE('',*,*,#4990,.T.);
#6436=ORIENTED_EDGE('',*,*,#4991,.F.);
#6437=ORIENTED_EDGE('',*,*,#4990,.F.);
#6438=ORIENTED_EDGE('',*,*,#4992,.F.);
#6439=ORIENTED_EDGE('',*,*,#4993,.T.);
#6440=ORIENTED_EDGE('',*,*,#4994,.F.);
#6441=ORIENTED_EDGE('',*,*,#4993,.F.);
#6442=ORIENTED_EDGE('',*,*,#4992,.T.);
#6443=ORIENTED_EDGE('',*,*,#4995,.T.);
#6444=ORIENTED_EDGE('',*,*,#4995,.F.);
#6445=ORIENTED_EDGE('',*,*,#4996,.T.);
#6446=ORIENTED_EDGE('',*,*,#4997,.T.);
#6447=ORIENTED_EDGE('',*,*,#4996,.F.);
#6448=ORIENTED_EDGE('',*,*,#4998,.F.);
#6449=ORIENTED_EDGE('',*,*,#4999,.T.);
#6450=ORIENTED_EDGE('',*,*,#5000,.T.);
#6451=ORIENTED_EDGE('',*,*,#4999,.F.);
#6452=ORIENTED_EDGE('',*,*,#4998,.T.);
#6453=ORIENTED_EDGE('',*,*,#4994,.T.);
#6454=ORIENTED_EDGE('',*,*,#4991,.T.);
#6455=ORIENTED_EDGE('',*,*,#4988,.T.);
#6456=ORIENTED_EDGE('',*,*,#4985,.T.);
#6457=ORIENTED_EDGE('',*,*,#4982,.T.);
#6458=ORIENTED_EDGE('',*,*,#5000,.F.);
#6459=ORIENTED_EDGE('',*,*,#4997,.F.);
#6460=ORIENTED_EDGE('',*,*,#4989,.T.);
#6461=ORIENTED_EDGE('',*,*,#4986,.T.);
#6462=ORIENTED_EDGE('',*,*,#4983,.T.);
#6463=ORIENTED_EDGE('',*,*,#4980,.T.);
#7622=CYLINDRICAL_SURFACE('',#9125,0.225);
#7623=CYLINDRICAL_SURFACE('',#9128,0.225);
#7624=CYLINDRICAL_SURFACE('',#9131,0.225);
#7625=CYLINDRICAL_SURFACE('',#9134,0.225);
#7626=CYLINDRICAL_SURFACE('',#9137,1.59);
#7627=CYLINDRICAL_SURFACE('',#9142,1.2);
#7628=CYLINDRICAL_SURFACE('',#9144,2.4);
#7882=ADVANCED_FACE('',(#1390),#7622,.F.);
#7883=ADVANCED_FACE('',(#1391),#7623,.F.);
#7884=ADVANCED_FACE('',(#1392),#7624,.F.);
#7885=ADVANCED_FACE('',(#1393),#7625,.F.);
#7886=ADVANCED_FACE('',(#1394),#7626,.T.);
#7887=ADVANCED_FACE('',(#1395,#873),#1042,.T.);
#7888=ADVANCED_FACE('',(#1396),#7627,.F.);
#7889=ADVANCED_FACE('',(#1397),#7628,.T.);
#7890=ADVANCED_FACE('',(#1398,#874,#875,#876,#877,#878),#1043,.T.);
#7891=ADVANCED_FACE('',(#1399,#879,#880,#881,#882,#883),#1044,.F.);
#8180=CLOSED_SHELL('',(#7882,#7883,#7884,#7885,#7886,#7887,#7888,#7889,
#7890,#7891));
#9124=AXIS2_PLACEMENT_3D('',#13313,#10797,#10798);
#9125=AXIS2_PLACEMENT_3D('',#13314,#10799,#10800);
#9126=AXIS2_PLACEMENT_3D('',#13316,#10801,#10802);
#9127=AXIS2_PLACEMENT_3D('',#13319,#10804,#10805);
#9128=AXIS2_PLACEMENT_3D('',#13320,#10806,#10807);
#9129=AXIS2_PLACEMENT_3D('',#13322,#10808,#10809);
#9130=AXIS2_PLACEMENT_3D('',#13325,#10811,#10812);
#9131=AXIS2_PLACEMENT_3D('',#13326,#10813,#10814);
#9132=AXIS2_PLACEMENT_3D('',#13328,#10815,#10816);
#9133=AXIS2_PLACEMENT_3D('',#13331,#10818,#10819);
#9134=AXIS2_PLACEMENT_3D('',#13332,#10820,#10821);
#9135=AXIS2_PLACEMENT_3D('',#13334,#10822,#10823);
#9136=AXIS2_PLACEMENT_3D('',#13337,#10825,#10826);
#9137=AXIS2_PLACEMENT_3D('',#13338,#10827,#10828);
#9138=AXIS2_PLACEMENT_3D('',#13340,#10829,#10830);
#9139=AXIS2_PLACEMENT_3D('',#13343,#10832,#10833);
#9140=AXIS2_PLACEMENT_3D('',#13344,#10834,#10835);
#9141=AXIS2_PLACEMENT_3D('',#13346,#10836,#10837);
#9142=AXIS2_PLACEMENT_3D('',#13347,#10838,#10839);
#9143=AXIS2_PLACEMENT_3D('',#13350,#10841,#10842);
#9144=AXIS2_PLACEMENT_3D('',#13351,#10843,#10844);
#9145=AXIS2_PLACEMENT_3D('',#13353,#10845,#10846);
#9146=AXIS2_PLACEMENT_3D('',#13356,#10848,#10849);
#9147=AXIS2_PLACEMENT_3D('',#13357,#10850,#10851);
#9148=AXIS2_PLACEMENT_3D('',#13358,#10852,#10853);
#10797=DIRECTION('axis',(0.,0.,1.));
#10798=DIRECTION('refdir',(1.,0.,0.));
#10799=DIRECTION('center_axis',(1.,0.,0.));
#10800=DIRECTION('ref_axis',(0.,0.,-1.));
#10801=DIRECTION('center_axis',(1.,0.,0.));
#10802=DIRECTION('ref_axis',(0.,0.,-1.));
#10803=DIRECTION('',(1.,0.,0.));
#10804=DIRECTION('center_axis',(-1.,0.,0.));
#10805=DIRECTION('ref_axis',(0.,0.,-1.));
#10806=DIRECTION('center_axis',(1.,0.,0.));
#10807=DIRECTION('ref_axis',(0.,0.,-1.));
#10808=DIRECTION('center_axis',(1.,0.,0.));
#10809=DIRECTION('ref_axis',(0.,0.,-1.));
#10810=DIRECTION('',(1.,0.,0.));
#10811=DIRECTION('center_axis',(-1.,0.,0.));
#10812=DIRECTION('ref_axis',(0.,0.,-1.));
#10813=DIRECTION('center_axis',(1.,0.,0.));
#10814=DIRECTION('ref_axis',(0.,0.,-1.));
#10815=DIRECTION('center_axis',(1.,0.,0.));
#10816=DIRECTION('ref_axis',(0.,0.,-1.));
#10817=DIRECTION('',(1.,0.,0.));
#10818=DIRECTION('center_axis',(-1.,0.,0.));
#10819=DIRECTION('ref_axis',(0.,0.,-1.));
#10820=DIRECTION('center_axis',(1.,0.,0.));
#10821=DIRECTION('ref_axis',(0.,0.,-1.));
#10822=DIRECTION('center_axis',(1.,0.,0.));
#10823=DIRECTION('ref_axis',(0.,0.,-1.));
#10824=DIRECTION('',(1.,0.,0.));
#10825=DIRECTION('center_axis',(-1.,0.,0.));
#10826=DIRECTION('ref_axis',(0.,0.,-1.));
#10827=DIRECTION('center_axis',(1.,0.,0.));
#10828=DIRECTION('ref_axis',(0.,0.,-1.));
#10829=DIRECTION('center_axis',(1.,0.,0.));
#10830=DIRECTION('ref_axis',(0.,0.,-1.));
#10831=DIRECTION('',(-1.,0.,0.));
#10832=DIRECTION('center_axis',(-1.,0.,0.));
#10833=DIRECTION('ref_axis',(0.,0.,-1.));
#10834=DIRECTION('center_axis',(1.,0.,0.));
#10835=DIRECTION('ref_axis',(0.,0.,-1.));
#10836=DIRECTION('center_axis',(-1.,0.,0.));
#10837=DIRECTION('ref_axis',(0.,0.,-1.));
#10838=DIRECTION('center_axis',(1.,0.,0.));
#10839=DIRECTION('ref_axis',(0.,0.,-1.));
#10840=DIRECTION('',(-1.,0.,0.));
#10841=DIRECTION('center_axis',(-1.,0.,0.));
#10842=DIRECTION('ref_axis',(0.,0.,-1.));
#10843=DIRECTION('center_axis',(1.,0.,0.));
#10844=DIRECTION('ref_axis',(0.,0.,-1.));
#10845=DIRECTION('center_axis',(1.,0.,0.));
#10846=DIRECTION('ref_axis',(0.,0.,-1.));
#10847=DIRECTION('',(-1.,0.,0.));
#10848=DIRECTION('center_axis',(1.,0.,0.));
#10849=DIRECTION('ref_axis',(0.,0.,-1.));
#10850=DIRECTION('center_axis',(1.,0.,0.));
#10851=DIRECTION('ref_axis',(0.,0.,-1.));
#10852=DIRECTION('center_axis',(1.,0.,0.));
#10853=DIRECTION('ref_axis',(0.,0.,-1.));
#13313=CARTESIAN_POINT('',(0.,0.,0.));
#13314=CARTESIAN_POINT('Origin',(4.4,1.51507575950825,5.51507575950825));
#13315=CARTESIAN_POINT('',(4.5,1.51507575950825,5.74007575950825));
#13316=CARTESIAN_POINT('Origin',(4.5,1.51507575950825,5.51507575950825));
#13317=CARTESIAN_POINT('',(4.7,1.51507575950825,5.74007575950825));
#13318=CARTESIAN_POINT('',(4.4,1.51507575950825,5.74007575950825));
#13319=CARTESIAN_POINT('Origin',(4.7,1.51507575950825,5.51507575950825));
#13320=CARTESIAN_POINT('Origin',(4.4,1.51507575950825,8.48492424049175));
#13321=CARTESIAN_POINT('',(4.5,1.51507575950825,8.70992424049175));
#13322=CARTESIAN_POINT('Origin',(4.5,1.51507575950825,8.48492424049175));
#13323=CARTESIAN_POINT('',(4.7,1.51507575950825,8.70992424049175));
#13324=CARTESIAN_POINT('',(4.4,1.51507575950825,8.70992424049175));
#13325=CARTESIAN_POINT('Origin',(4.7,1.51507575950825,8.48492424049175));
#13326=CARTESIAN_POINT('Origin',(4.4,4.48492424049175,8.48492424049175));
#13327=CARTESIAN_POINT('',(4.5,4.48492424049175,8.70992424049175));
#13328=CARTESIAN_POINT('Origin',(4.5,4.48492424049175,8.48492424049175));
#13329=CARTESIAN_POINT('',(4.7,4.48492424049175,8.70992424049175));
#13330=CARTESIAN_POINT('',(4.4,4.48492424049175,8.70992424049175));
#13331=CARTESIAN_POINT('Origin',(4.7,4.48492424049175,8.48492424049175));
#13332=CARTESIAN_POINT('Origin',(4.4,4.48492424049175,5.51507575950825));
#13333=CARTESIAN_POINT('',(4.5,4.48492424049175,5.74007575950825));
#13334=CARTESIAN_POINT('Origin',(4.5,4.48492424049175,5.51507575950825));
#13335=CARTESIAN_POINT('',(4.7,4.48492424049175,5.74007575950825));
#13336=CARTESIAN_POINT('',(4.4,4.48492424049175,5.74007575950825));
#13337=CARTESIAN_POINT('Origin',(4.7,4.48492424049175,5.51507575950825));
#13338=CARTESIAN_POINT('Origin',(4.7,3.,7.));
#13339=CARTESIAN_POINT('',(5.,3.,8.59));
#13340=CARTESIAN_POINT('Origin',(5.,3.,7.));
#13341=CARTESIAN_POINT('',(4.7,3.,8.59));
#13342=CARTESIAN_POINT('',(4.7,3.,8.59));
#13343=CARTESIAN_POINT('Origin',(4.7,3.,7.));
#13344=CARTESIAN_POINT('Origin',(5.,3.,7.));
#13345=CARTESIAN_POINT('',(5.,3.,8.2));
#13346=CARTESIAN_POINT('Origin',(5.,3.,7.));
#13347=CARTESIAN_POINT('Origin',(4.5,3.,7.));
#13348=CARTESIAN_POINT('',(4.5,3.,8.2));
#13349=CARTESIAN_POINT('',(4.5,3.,8.2));
#13350=CARTESIAN_POINT('Origin',(4.5,3.,7.));
#13351=CARTESIAN_POINT('Origin',(4.5,3.,7.));
#13352=CARTESIAN_POINT('',(4.7,3.,9.4));
#13353=CARTESIAN_POINT('Origin',(4.7,3.,7.));
#13354=CARTESIAN_POINT('',(4.5,3.,9.4));
#13355=CARTESIAN_POINT('',(4.5,3.,9.4));
#13356=CARTESIAN_POINT('Origin',(4.5,3.,7.));
#13357=CARTESIAN_POINT('Origin',(4.7,3.,7.));
#13358=CARTESIAN_POINT('Origin',(4.5,3.,7.));
#16957=UNCERTAINTY_MEASURE_WITH_UNIT(LENGTH_MEASURE(0.001),#17047,
'DISTANCE_ACCURACY_VALUE',
'Maximum model space distance between geometric entities at asserted c
onnectivities');
#16993=UNCERTAINTY_MEASURE_WITH_UNIT(LENGTH_MEASURE(0.001),#17047,
'DISTANCE_ACCURACY_VALUE',
'Maximum model space distance between geometric entities at asserted c
onnectivities');
#17010=(
GEOMETRIC_REPRESENTATION_CONTEXT(3)
GLOBAL_UNCERTAINTY_ASSIGNED_CONTEXT((#16957))
GLOBAL_UNIT_ASSIGNED_CONTEXT((#17047,#17049,#17050))
REPRESENTATION_CONTEXT('','3D')
);
#17046=(
GEOMETRIC_REPRESENTATION_CONTEXT(3)
GLOBAL_UNCERTAINTY_ASSIGNED_CONTEXT((#16993))
GLOBAL_UNIT_ASSIGNED_CONTEXT((#17047,#17049,#17050))
REPRESENTATION_CONTEXT('','3D')
);
#17047=(
LENGTH_UNIT()
NAMED_UNIT(*)
SI_UNIT(.CENTI.,.METRE.)
);
#17049=(
NAMED_UNIT(*)
PLANE_ANGLE_UNIT()
SI_UNIT($,.RADIAN.)
);
#17050=(
NAMED_UNIT(*)
SI_UNIT($,.STERADIAN.)
SOLID_ANGLE_UNIT()
);
#17067=SHAPE_DEFINITION_REPRESENTATION(#17119,#17274);
#17119=PRODUCT_DEFINITION_SHAPE('',$,#17327);
#17274=SHAPE_REPRESENTATION('',(#9124),#17010);
#17310=PRODUCT_DEFINITION_CONTEXT('part definition',#17468,'design');
#17327=PRODUCT_DEFINITION('Bearing cap (6)','Bearing cap (6)',#17379,#17310);
#17379=PRODUCT_DEFINITION_FORMATION('',$,#17486);
#17468=APPLICATION_CONTEXT(
'Core Data for Automotive Mechanical Design Process');
#17469=PRODUCT_CONTEXT('part definition',#17468,'mechanical');
#17486=PRODUCT('Bearing cap (6)','Bearing cap (6)','Bearing cap (6)',(#17469));
#17585=COLOUR_RGB('Grey',0.48,0.52,0.57);
#17586=FILL_AREA_STYLE_COLOUR('',#17585);
#17587=FILL_AREA_STYLE('',(#17586));
#17588=SURFACE_STYLE_FILL_AREA(#17587);
#17589=SURFACE_SIDE_STYLE('',(#17588));
#17590=SURFACE_STYLE_USAGE(.BOTH.,#17589);
#17591=PRESENTATION_STYLE_ASSIGNMENT((#17590));
ENDSEC;
END-ISO-10303-21;
